ISO-10303-21;
HEADER;
FILE_DESCRIPTION((''),'2;1');
FILE_NAME('GATE_HOUSING_BOLT_M8x30.step','2026-10-01T22:06:14-07:00',(''),(''),'','','');
FILE_SCHEMA (('AUTOMOTIVE_DESIGN { 1 0 10303 214 3 1 1 }'));
ENDSEC;
DATA;
#10=MECHANICAL_DESIGN_GEOMETRIC_PRESENTATION_REPRESENTATION('',(#1032),#50440);
#931=SHAPE_REPRESENTATION_RELATIONSHIP('SRR','None',#50666,#976) ;
#976=ADVANCED_BREP_SHAPE_REPRESENTATION('',(#1085),#50435) ;
#1032=STYLED_ITEM('',(#50883),#1085) ;
#1085=MANIFOLD_SOLID_BREP('GATE_HOUSING_BOLT_M8x30',#28710) ;
#1403=FACE_BOUND('',#5693,.T.) ;
#2314=PLANE('',#32236) ;
#2315=PLANE('',#32237) ;
#2316=PLANE('',#32238) ;
#2317=PLANE('',#32239) ;
#2318=PLANE('',#32240) ;
#2319=PLANE('',#32241) ;
#2320=PLANE('',#32242) ;
#2321=PLANE('',#32243) ;
#2322=PLANE('',#32244) ;
#3838=FACE_OUTER_BOUND('',#5683,.T.) ;
#3839=FACE_OUTER_BOUND('',#5684,.T.) ;
#3840=FACE_OUTER_BOUND('',#5685,.T.) ;
#3841=FACE_OUTER_BOUND('',#5686,.T.) ;
#3842=FACE_OUTER_BOUND('',#5687,.T.) ;
#3843=FACE_OUTER_BOUND('',#5688,.T.) ;
#3844=FACE_OUTER_BOUND('',#5689,.T.) ;
#3845=FACE_OUTER_BOUND('',#5690,.T.) ;
#3846=FACE_OUTER_BOUND('',#5691,.T.) ;
#3847=FACE_OUTER_BOUND('',#5692,.T.) ;
#5683=EDGE_LOOP('',(#26391,#26392,#26393,#26394)) ;
#5684=EDGE_LOOP('',(#26395)) ;
#5685=EDGE_LOOP('',(#26396,#26397,#26398,#26399)) ;
#5686=EDGE_LOOP('',(#26400,#26401,#26402,#26403)) ;
#5687=EDGE_LOOP('',(#26404,#26405,#26406,#26407,#26408,#26409)) ;
#5688=EDGE_LOOP('',(#26410,#26411,#26412,#26413)) ;
#5689=EDGE_LOOP('',(#26414,#26415,#26416,#26417)) ;
#5690=EDGE_LOOP('',(#26418,#26419,#26420,#26421)) ;
#5691=EDGE_LOOP('',(#26422,#26423,#26424,#26425)) ;
#5692=EDGE_LOOP('',(#26426,#26427,#26428,#26429,#26430,#26431)) ;
#5693=EDGE_LOOP('',(#26432)) ;
#8161=LINE('',#49995,#10633) ;
#8162=LINE('',#50001,#10634) ;
#8163=LINE('',#50003,#10635) ;
#8164=LINE('',#50005,#10636) ;
#8165=LINE('',#50006,#10637) ;
#8166=LINE('',#50010,#10638) ;
#8167=LINE('',#50012,#10639) ;
#8168=LINE('',#50014,#10640) ;
#8169=LINE('',#50015,#10641) ;
#8170=LINE('',#50018,#10642) ;
#8171=LINE('',#50019,#10643) ;
#8172=LINE('',#50021,#10644) ;
#8173=LINE('',#50022,#10645) ;
#8174=LINE('',#50025,#10646) ;
#8175=LINE('',#50026,#10647) ;
#8176=LINE('',#50029,#10648) ;
#8177=LINE('',#50030,#10649) ;
#8178=LINE('',#50032,#10650) ;
#8179=LINE('',#50034,#10651) ;
#10633=VECTOR('',#40856,0.4) ;
#10634=VECTOR('',#40863,1.) ;
#10635=VECTOR('',#40864,1.) ;
#10636=VECTOR('',#40865,1.) ;
#10637=VECTOR('',#40866,1.) ;
#10638=VECTOR('',#40869,1.) ;
#10639=VECTOR('',#40870,1.) ;
#10640=VECTOR('',#40871,1.) ;
#10641=VECTOR('',#40872,1.) ;
#10642=VECTOR('',#40875,1.) ;
#10643=VECTOR('',#40876,1.) ;
#10644=VECTOR('',#40877,1.) ;
#10645=VECTOR('',#40878,1.) ;
#10646=VECTOR('',#40881,1.) ;
#10647=VECTOR('',#40882,1.) ;
#10648=VECTOR('',#40885,1.) ;
#10649=VECTOR('',#40886,1.) ;
#10650=VECTOR('',#40889,1.) ;
#10651=VECTOR('',#40892,1.) ;
#11806=CIRCLE('',#32234,0.4) ;
#11807=CIRCLE('',#32235,0.4) ;
#14476=VERTEX_POINT('',#49992) ;
#14477=VERTEX_POINT('',#49994) ;
#14478=VERTEX_POINT('',#49999) ;
#14479=VERTEX_POINT('',#50000) ;
#14480=VERTEX_POINT('',#50002) ;
#14481=VERTEX_POINT('',#50004) ;
#14482=VERTEX_POINT('',#50008) ;
#14483=VERTEX_POINT('',#50009) ;
#14484=VERTEX_POINT('',#50011) ;
#14485=VERTEX_POINT('',#50013) ;
#14486=VERTEX_POINT('',#50017) ;
#14487=VERTEX_POINT('',#50020) ;
#14488=VERTEX_POINT('',#50024) ;
#14489=VERTEX_POINT('',#50028) ;
#18461=EDGE_CURVE('',#14476,#14476,#11806,.T.) ;
#18462=EDGE_CURVE('',#14476,#14477,#8161,.T.) ;
#18463=EDGE_CURVE('',#14477,#14477,#11807,.T.) ;
#18464=EDGE_CURVE('',#14478,#14479,#8162,.T.) ;
#18465=EDGE_CURVE('',#14478,#14480,#8163,.T.) ;
#18466=EDGE_CURVE('',#14481,#14480,#8164,.T.) ;
#18467=EDGE_CURVE('',#14481,#14479,#8165,.T.) ;
#18468=EDGE_CURVE('',#14482,#14483,#8166,.T.) ;
#18469=EDGE_CURVE('',#14482,#14484,#8167,.T.) ;
#18470=EDGE_CURVE('',#14485,#14484,#8168,.T.) ;
#18471=EDGE_CURVE('',#14485,#14483,#8169,.T.) ;
#18472=EDGE_CURVE('',#14486,#14478,#8170,.T.) ;
#18473=EDGE_CURVE('',#14484,#14486,#8171,.T.) ;
#18474=EDGE_CURVE('',#14487,#14482,#8172,.T.) ;
#18475=EDGE_CURVE('',#14480,#14487,#8173,.T.) ;
#18476=EDGE_CURVE('',#14486,#14488,#8174,.T.) ;
#18477=EDGE_CURVE('',#14479,#14488,#8175,.T.) ;
#18478=EDGE_CURVE('',#14487,#14489,#8176,.T.) ;
#18479=EDGE_CURVE('',#14483,#14489,#8177,.T.) ;
#18480=EDGE_CURVE('',#14488,#14485,#8178,.T.) ;
#18481=EDGE_CURVE('',#14489,#14481,#8179,.T.) ;
#26391=ORIENTED_EDGE('',*,*,#18461,.F.) ;
#26392=ORIENTED_EDGE('',*,*,#18462,.T.) ;
#26393=ORIENTED_EDGE('',*,*,#18463,.F.) ;
#26394=ORIENTED_EDGE('',*,*,#18462,.F.) ;
#26395=ORIENTED_EDGE('',*,*,#18461,.T.) ;
#26396=ORIENTED_EDGE('',*,*,#18464,.F.) ;
#26397=ORIENTED_EDGE('',*,*,#18465,.T.) ;
#26398=ORIENTED_EDGE('',*,*,#18466,.F.) ;
#26399=ORIENTED_EDGE('',*,*,#18467,.T.) ;
#26400=ORIENTED_EDGE('',*,*,#18468,.F.) ;
#26401=ORIENTED_EDGE('',*,*,#18469,.T.) ;
#26402=ORIENTED_EDGE('',*,*,#18470,.F.) ;
#26403=ORIENTED_EDGE('',*,*,#18471,.T.) ;
#26404=ORIENTED_EDGE('',*,*,#18465,.F.) ;
#26405=ORIENTED_EDGE('',*,*,#18472,.F.) ;
#26406=ORIENTED_EDGE('',*,*,#18473,.F.) ;
#26407=ORIENTED_EDGE('',*,*,#18469,.F.) ;
#26408=ORIENTED_EDGE('',*,*,#18474,.F.) ;
#26409=ORIENTED_EDGE('',*,*,#18475,.F.) ;
#26410=ORIENTED_EDGE('',*,*,#18476,.F.) ;
#26411=ORIENTED_EDGE('',*,*,#18472,.T.) ;
#26412=ORIENTED_EDGE('',*,*,#18464,.T.) ;
#26413=ORIENTED_EDGE('',*,*,#18477,.T.) ;
#26414=ORIENTED_EDGE('',*,*,#18478,.F.) ;
#26415=ORIENTED_EDGE('',*,*,#18474,.T.) ;
#26416=ORIENTED_EDGE('',*,*,#18468,.T.) ;
#26417=ORIENTED_EDGE('',*,*,#18479,.T.) ;
#26418=ORIENTED_EDGE('',*,*,#18476,.T.) ;
#26419=ORIENTED_EDGE('',*,*,#18480,.T.) ;
#26420=ORIENTED_EDGE('',*,*,#18470,.T.) ;
#26421=ORIENTED_EDGE('',*,*,#18473,.T.) ;
#26422=ORIENTED_EDGE('',*,*,#18466,.T.) ;
#26423=ORIENTED_EDGE('',*,*,#18475,.T.) ;
#26424=ORIENTED_EDGE('',*,*,#18478,.T.) ;
#26425=ORIENTED_EDGE('',*,*,#18481,.T.) ;
#26426=ORIENTED_EDGE('',*,*,#18467,.F.) ;
#26427=ORIENTED_EDGE('',*,*,#18481,.F.) ;
#26428=ORIENTED_EDGE('',*,*,#18479,.F.) ;
#26429=ORIENTED_EDGE('',*,*,#18471,.F.) ;
#26430=ORIENTED_EDGE('',*,*,#18480,.F.) ;
#26431=ORIENTED_EDGE('',*,*,#18477,.F.) ;
#26432=ORIENTED_EDGE('',*,*,#18463,.T.) ;
#27056=CYLINDRICAL_SURFACE('',#32233,0.4) ;
#28573=ADVANCED_FACE('',(#3838),#27056,.T.) ;
#28574=ADVANCED_FACE('',(#3839),#2314,.T.) ;
#28575=ADVANCED_FACE('',(#3840),#2315,.F.) ;
#28576=ADVANCED_FACE('',(#3841),#2316,.F.) ;
#28577=ADVANCED_FACE('',(#3842),#2317,.T.) ;
#28578=ADVANCED_FACE('',(#3843),#2318,.F.) ;
#28579=ADVANCED_FACE('',(#3844),#2319,.F.) ;
#28580=ADVANCED_FACE('',(#3845),#2320,.F.) ;
#28581=ADVANCED_FACE('',(#3846),#2321,.F.) ;
#28582=ADVANCED_FACE('',(#3847,#1403),#2322,.T.) ;
#28710=CLOSED_SHELL('',(#28573,#28574,#28575,#28576,#28577,#28578,#28579,
#28580,#28581,#28582)) ;
#32232=AXIS2_PLACEMENT_3D('',#49990,#40850,#40851) ;
#32233=AXIS2_PLACEMENT_3D('',#49991,#40852,#40853) ;
#32234=AXIS2_PLACEMENT_3D('',#49993,#40854,#40855) ;
#32235=AXIS2_PLACEMENT_3D('',#49996,#40857,#40858) ;
#32236=AXIS2_PLACEMENT_3D('',#49997,#40859,#40860) ;
#32237=AXIS2_PLACEMENT_3D('',#49998,#40861,#40862) ;
#32238=AXIS2_PLACEMENT_3D('',#50007,#40867,#40868) ;
#32239=AXIS2_PLACEMENT_3D('',#50016,#40873,#40874) ;
#32240=AXIS2_PLACEMENT_3D('',#50023,#40879,#40880) ;
#32241=AXIS2_PLACEMENT_3D('',#50027,#40883,#40884) ;
#32242=AXIS2_PLACEMENT_3D('',#50031,#40887,#40888) ;
#32243=AXIS2_PLACEMENT_3D('',#50033,#40890,#40891) ;
#32244=AXIS2_PLACEMENT_3D('',#50035,#40893,#40894) ;
#40850=DIRECTION('axis',(0.,0.,1.)) ;
#40851=DIRECTION('refdir',(1.,0.,0.)) ;
#40852=DIRECTION('center_axis',(0.,0.,-1.)) ;
#40853=DIRECTION('ref_axis',(1.,0.,0.)) ;
#40854=DIRECTION('center_axis',(0.,0.,-1.)) ;
#40855=DIRECTION('ref_axis',(1.,0.,0.)) ;
#40856=DIRECTION('',(0.,0.,1.)) ;
#40857=DIRECTION('center_axis',(0.,0.,1.)) ;
#40858=DIRECTION('ref_axis',(1.,0.,0.)) ;
#40859=DIRECTION('center_axis',(0.,0.,-1.)) ;
#40860=DIRECTION('ref_axis',(1.,0.,0.)) ;
#40861=DIRECTION('center_axis',(-0.5,-0.866025403784439,0.)) ;
#40862=DIRECTION('ref_axis',(-0.866025403784439,0.5,0.)) ;
#40863=DIRECTION('',(0.,0.,-1.)) ;
#40864=DIRECTION('',(0.866025403784439,-0.5,0.)) ;
#40865=DIRECTION('',(0.,0.,1.)) ;
#40866=DIRECTION('',(-0.866025403784439,0.5,0.)) ;
#40867=DIRECTION('center_axis',(0.5,0.866025403784439,0.)) ;
#40868=DIRECTION('ref_axis',(0.866025403784439,-0.5,0.)) ;
#40869=DIRECTION('',(0.,0.,-1.)) ;
#40870=DIRECTION('',(-0.866025403784439,0.5,0.)) ;
#40871=DIRECTION('',(0.,0.,1.)) ;
#40872=DIRECTION('',(0.866025403784439,-0.5,0.)) ;
#40873=DIRECTION('center_axis',(0.,0.,1.)) ;
#40874=DIRECTION('ref_axis',(-1.,0.,0.)) ;
#40875=DIRECTION('',(0.866025403784439,0.5,0.)) ;
#40876=DIRECTION('',(0.,1.,0.)) ;
#40877=DIRECTION('',(-0.866025403784439,-0.5,0.)) ;
#40878=DIRECTION('',(0.,-1.,0.)) ;
#40879=DIRECTION('center_axis',(0.5,-0.866025403784439,0.)) ;
#40880=DIRECTION('ref_axis',(-0.866025403784439,-0.5,0.)) ;
#40881=DIRECTION('',(0.,0.,-1.)) ;
#40882=DIRECTION('',(-0.866025403784439,-0.5,0.)) ;
#40883=DIRECTION('center_axis',(-0.5,0.866025403784439,0.)) ;
#40884=DIRECTION('ref_axis',(0.866025403784439,0.5,0.)) ;
#40885=DIRECTION('',(0.,0.,-1.)) ;
#40886=DIRECTION('',(0.866025403784439,0.5,0.)) ;
#40887=DIRECTION('center_axis',(1.,0.,0.)) ;
#40888=DIRECTION('ref_axis',(0.,-1.,0.)) ;
#40889=DIRECTION('',(0.,-1.,0.)) ;
#40890=DIRECTION('center_axis',(-1.,0.,0.)) ;
#40891=DIRECTION('ref_axis',(0.,1.,0.)) ;
#40892=DIRECTION('',(0.,1.,0.)) ;
#40893=DIRECTION('center_axis',(0.,0.,-1.)) ;
#40894=DIRECTION('ref_axis',(1.,0.,0.)) ;
#49990=CARTESIAN_POINT('',(0.,0.,0.)) ;
#49991=CARTESIAN_POINT('Origin',(0.,0.,-1.5)) ;
#49992=CARTESIAN_POINT('',(-0.4,4.89858719658941E-17,-3.)) ;
#49993=CARTESIAN_POINT('Origin',(0.,0.,-3.)) ;
#49994=CARTESIAN_POINT('',(-0.4,4.89858719658941E-17,0.)) ;
#49995=CARTESIAN_POINT('',(-0.4,4.89858719658941E-17,-1.5)) ;
#49996=CARTESIAN_POINT('Origin',(0.,0.,0.)) ;
#49997=CARTESIAN_POINT('Origin',(0.,0.,-3.)) ;
#49998=CARTESIAN_POINT('Origin',(0.325,0.562916512459885,0.265)) ;
#49999=CARTESIAN_POINT('',(0.,0.750555349946514,0.53)) ;
#50000=CARTESIAN_POINT('',(0.,0.750555349946514,0.)) ;
#50001=CARTESIAN_POINT('',(0.,0.750555349946514,0.265)) ;
#50002=CARTESIAN_POINT('',(0.65,0.375277674973257,0.53)) ;
#50003=CARTESIAN_POINT('',(0.325,0.562916512459885,0.53)) ;
#50004=CARTESIAN_POINT('',(0.65,0.375277674973257,0.)) ;
#50005=CARTESIAN_POINT('',(0.65,0.375277674973257,0.265)) ;
#50006=CARTESIAN_POINT('',(0.325,0.562916512459885,0.)) ;
#50007=CARTESIAN_POINT('Origin',(-0.325,-0.562916512459885,0.265)) ;
#50008=CARTESIAN_POINT('',(0.,-0.750555349946514,0.53)) ;
#50009=CARTESIAN_POINT('',(0.,-0.750555349946514,0.)) ;
#50010=CARTESIAN_POINT('',(0.,-0.750555349946514,0.265)) ;
#50011=CARTESIAN_POINT('',(-0.65,-0.375277674973257,0.53)) ;
#50012=CARTESIAN_POINT('',(-0.325,-0.562916512459885,0.53)) ;
#50013=CARTESIAN_POINT('',(-0.65,-0.375277674973257,0.)) ;
#50014=CARTESIAN_POINT('',(-0.65,-0.375277674973257,0.265)) ;
#50015=CARTESIAN_POINT('',(-0.325,-0.562916512459885,0.)) ;
#50016=CARTESIAN_POINT('Origin',(0.,0.,0.53)) ;
#50017=CARTESIAN_POINT('',(-0.65,0.375277674973257,0.53)) ;
#50018=CARTESIAN_POINT('',(-0.325,0.562916512459885,0.53)) ;
#50019=CARTESIAN_POINT('',(-0.65,0.,0.53)) ;
#50020=CARTESIAN_POINT('',(0.65,-0.375277674973257,0.53)) ;
#50021=CARTESIAN_POINT('',(0.325,-0.562916512459885,0.53)) ;
#50022=CARTESIAN_POINT('',(0.65,0.,0.53)) ;
#50023=CARTESIAN_POINT('Origin',(-0.325,0.562916512459885,0.265)) ;
#50024=CARTESIAN_POINT('',(-0.65,0.375277674973257,0.)) ;
#50025=CARTESIAN_POINT('',(-0.65,0.375277674973257,0.265)) ;
#50026=CARTESIAN_POINT('',(-0.325,0.562916512459885,0.)) ;
#50027=CARTESIAN_POINT('Origin',(0.325,-0.562916512459885,0.265)) ;
#50028=CARTESIAN_POINT('',(0.65,-0.375277674973257,0.)) ;
#50029=CARTESIAN_POINT('',(0.65,-0.375277674973257,0.265)) ;
#50030=CARTESIAN_POINT('',(0.325,-0.562916512459885,0.)) ;
#50031=CARTESIAN_POINT('Origin',(-0.65,0.,0.265)) ;
#50032=CARTESIAN_POINT('',(-0.65,0.,0.)) ;
#50033=CARTESIAN_POINT('Origin',(0.65,0.,0.265)) ;
#50034=CARTESIAN_POINT('',(0.65,0.,0.)) ;
#50035=CARTESIAN_POINT('Origin',(0.,0.,0.)) ;
#50382=UNCERTAINTY_MEASURE_WITH_UNIT(LENGTH_MEASURE(0.001),#50441,
'DISTANCE_ACCURACY_VALUE',
'Maximum model space distance between geometric entities at asserted c
onnectivities') ;
#50387=UNCERTAINTY_MEASURE_WITH_UNIT(LENGTH_MEASURE(0.001),#50441,
'DISTANCE_ACCURACY_VALUE',
'Maximum model space distance between geometric entities at asserted c
onnectivities') ;
#50435=(
GEOMETRIC_REPRESENTATION_CONTEXT(3)
GLOBAL_UNCERTAINTY_ASSIGNED_CONTEXT((#50382))
GLOBAL_UNIT_ASSIGNED_CONTEXT((#50441,#50443,#50444))
REPRESENTATION_CONTEXT('','3D')
) ;
#50440=(
GEOMETRIC_REPRESENTATION_CONTEXT(3)
GLOBAL_UNCERTAINTY_ASSIGNED_CONTEXT((#50387))
GLOBAL_UNIT_ASSIGNED_CONTEXT((#50441,#50443,#50444))
REPRESENTATION_CONTEXT('','3D')
) ;
#50441=(
LENGTH_UNIT()
NAMED_UNIT(*)
SI_UNIT(.CENTI.,.METRE.)
) ;
#50443=(
NAMED_UNIT(*)
PLANE_ANGLE_UNIT()
SI_UNIT($,.RADIAN.)
) ;
#50444=(
NAMED_UNIT(*)
SI_UNIT($,.STERADIAN.)
SOLID_ANGLE_UNIT()
) ;
#50492=SHAPE_DEFINITION_REPRESENTATION(#50588,#50666) ;
#50588=PRODUCT_DEFINITION_SHAPE('',$,#50719) ;
#50666=SHAPE_REPRESENTATION('',(#32232),#50435) ;
#50671=PRODUCT_DEFINITION_CONTEXT('part definition',#50829,'design') ;
#50719=PRODUCT_DEFINITION('GATE_HOUSING_BOLT_M8x30',
'GATE_HOUSING_BOLT_M8x30',#50771,#50671) ;
#50771=PRODUCT_DEFINITION_FORMATION('',$,#50878) ;
#50829=APPLICATION_CONTEXT(
'Core Data for Automotive Mechanical Design Process') ;
#50830=PRODUCT_CONTEXT('part definition',#50829,'mechanical') ;
#50878=PRODUCT('GATE_HOUSING_BOLT_M8x30','GATE_HOUSING_BOLT_M8x30',$,(#50830)) ;
#50883=PRESENTATION_STYLE_ASSIGNMENT((#50890)) ;
#50890=SURFACE_STYLE_USAGE(.BOTH.,#50897) ;
#50897=SURFACE_SIDE_STYLE('',(#50904)) ;
#50904=SURFACE_STYLE_FILL_AREA(#50911) ;
#50911=FILL_AREA_STYLE('Steel - Satin',(#50918)) ;
#50918=FILL_AREA_STYLE_COLOUR('Steel - Satin',#50925) ;
#50925=COLOUR_RGB('Steel - Satin', 0.31764706, 0.68627451, 0.89019608) ;
ENDSEC;
END-ISO-10303-21;
